ISO-10303-21;
HEADER;
/* Generated by software containing ST-Developer
 * from STEP Tools, Inc. (www.steptools.com) 
 */

FILE_DESCRIPTION(
/* description */ ('PAT-015'),
/* implementation_level */ '2;1');

FILE_NAME(
/* name */ 'Cap Screw - M5x20.step',
/* time_stamp */ '2026-10-29T16:03:43-07:00',
/* author */ (''),
/* organization */ (''),
/* preprocessor_version */ 'ST-DEVELOPER v20.2',
/* originating_system */ 'Autodesk Translation Framework v15.17.0.0',
/* authorisation */ '');

FILE_SCHEMA (('AUTOMOTIVE_DESIGN { 1 0 10303 214 3 1 1 }'));
ENDSEC;

DATA;
#10=MECHANICAL_DESIGN_GEOMETRIC_PRESENTATION_REPRESENTATION('',(#248),#10266);
#163=ORIENTED_CLOSED_SHELL('',*,#4708,.F.);
#165=BREP_WITH_VOIDS('Body1',#4707,(#163));
#170=CONICAL_SURFACE('',#5416,0.4,0.785398163397448);
#171=CONICAL_SURFACE('',#5420,0.41,0.785398163397448);
#172=CONICAL_SURFACE('',#5424,0.26,0.463647609000806);
#173=CONICAL_SURFACE('',#5428,0.225,0.785398163397448);
#200=SHAPE_REPRESENTATION_RELATIONSHIP('SRR','None',#10371,#223);
#223=ADVANCED_BREP_SHAPE_REPRESENTATION('',(#165),#10259);
#248=STYLED_ITEM('',(#10554),#165);
#411=FACE_BOUND('',#1192,.T.);
#524=PLANE('',#5414);
#525=PLANE('',#5422);
#526=PLANE('',#5430);
#527=PLANE('',#5431);
#528=PLANE('',#5432);
#529=PLANE('',#5433);
#530=PLANE('',#5434);
#531=PLANE('',#5435);
#532=PLANE('',#5436);
#533=PLANE('',#5437);
#534=PLANE('',#5438);
#785=FACE_OUTER_BOUND('',#1187,.T.);
#786=FACE_OUTER_BOUND('',#1188,.T.);
#787=FACE_OUTER_BOUND('',#1189,.T.);
#788=FACE_OUTER_BOUND('',#1190,.T.);
#789=FACE_OUTER_BOUND('',#1191,.T.);
#790=FACE_OUTER_BOUND('',#1193,.T.);
#791=FACE_OUTER_BOUND('',#1194,.T.);
#792=FACE_OUTER_BOUND('',#1195,.T.);
#793=FACE_OUTER_BOUND('',#1196,.T.);
#794=FACE_OUTER_BOUND('',#1197,.T.);
#795=FACE_OUTER_BOUND('',#1198,.T.);
#796=FACE_OUTER_BOUND('',#1199,.T.);
#797=FACE_OUTER_BOUND('',#1200,.T.);
#798=FACE_OUTER_BOUND('',#1201,.T.);
#799=FACE_OUTER_BOUND('',#1202,.T.);
#800=FACE_OUTER_BOUND('',#1203,.T.);
#801=FACE_OUTER_BOUND('',#1204,.T.);
#1187=EDGE_LOOP('',(#4017));
#1188=EDGE_LOOP('',(#4018,#4019,#4020,#4021));
#1189=EDGE_LOOP('',(#4022,#4023,#4024,#4025));
#1190=EDGE_LOOP('',(#4026,#4027,#4028,#4029));
#1191=EDGE_LOOP('',(#4030));
#1192=EDGE_LOOP('',(#4031));
#1193=EDGE_LOOP('',(#4032,#4033,#4034,#4035));
#1194=EDGE_LOOP('',(#4036,#4037,#4038,#4039));
#1195=EDGE_LOOP('',(#4040,#4041,#4042,#4043));
#1196=EDGE_LOOP('',(#4044));
#1197=EDGE_LOOP('',(#4045,#4046,#4047,#4048));
#1198=EDGE_LOOP('',(#4049,#4050,#4051,#4052));
#1199=EDGE_LOOP('',(#4053,#4054,#4055,#4056));
#1200=EDGE_LOOP('',(#4057,#4058,#4059,#4060));
#1201=EDGE_LOOP('',(#4061,#4062,#4063,#4064));
#1202=EDGE_LOOP('',(#4065,#4066,#4067,#4068));
#1203=EDGE_LOOP('',(#4069,#4070,#4071,#4072,#4073,#4074));
#1204=EDGE_LOOP('',(#4075,#4076,#4077,#4078,#4079,#4080));
#1510=LINE('',#9865,#1790);
#1511=LINE('',#9869,#1791);
#1512=LINE('',#9873,#1792);
#1513=LINE('',#9880,#1793);
#1514=LINE('',#9884,#1794);
#1515=LINE('',#9888,#1795);
#1516=LINE('',#9893,#1796);
#1517=LINE('',#9895,#1797);
#1518=LINE('',#9897,#1798);
#1519=LINE('',#9898,#1799);
#1520=LINE('',#9901,#1800);
#1521=LINE('',#9903,#1801);
#1522=LINE('',#9904,#1802);
#1523=LINE('',#9907,#1803);
#1524=LINE('',#9909,#1804);
#1525=LINE('',#9910,#1805);
#1526=LINE('',#9913,#1806);
#1527=LINE('',#9915,#1807);
#1528=LINE('',#9916,#1808);
#1529=LINE('',#9919,#1809);
#1530=LINE('',#9921,#1810);
#1531=LINE('',#9922,#1811);
#1532=LINE('',#9924,#1812);
#1533=LINE('',#9925,#1813);
#1790=VECTOR('',#6639,0.4);
#1791=VECTOR('',#6644,0.425);
#1792=VECTOR('',#6649,0.41);
#1793=VECTOR('',#6658,0.26);
#1794=VECTOR('',#6663,0.25);
#1795=VECTOR('',#6668,0.225);
#1796=VECTOR('',#6673,1.);
#1797=VECTOR('',#6674,1.);
#1798=VECTOR('',#6675,1.);
#1799=VECTOR('',#6676,1.);
#1800=VECTOR('',#6679,1.);
#1801=VECTOR('',#6680,1.);
#1802=VECTOR('',#6681,1.);
#1803=VECTOR('',#6684,1.);
#1804=VECTOR('',#6685,1.);
#1805=VECTOR('',#6686,1.);
#1806=VECTOR('',#6689,1.);
#1807=VECTOR('',#6690,1.);
#1808=VECTOR('',#6691,1.);
#1809=VECTOR('',#6694,1.);
#1810=VECTOR('',#6695,1.);
#1811=VECTOR('',#6696,1.);
#1812=VECTOR('',#6699,1.);
#1813=VECTOR('',#6700,1.);
#2082=CIRCLE('',#5415,0.375);
#2083=CIRCLE('',#5417,0.425);
#2084=CIRCLE('',#5419,0.425);
#2085=CIRCLE('',#5421,0.395);
#2086=CIRCLE('',#5423,0.27);
#2087=CIRCLE('',#5425,0.24505);
#2088=CIRCLE('',#5427,0.24505);
#2089=CIRCLE('',#5429,0.2);
#2419=VERTEX_POINT('',#9860);
#2420=VERTEX_POINT('',#9863);
#2421=VERTEX_POINT('',#9867);
#2422=VERTEX_POINT('',#9871);
#2423=VERTEX_POINT('',#9875);
#2424=VERTEX_POINT('',#9878);
#2425=VERTEX_POINT('',#9882);
#2426=VERTEX_POINT('',#9886);
#2427=VERTEX_POINT('',#9891);
#2428=VERTEX_POINT('',#9892);
#2429=VERTEX_POINT('',#9894);
#2430=VERTEX_POINT('',#9896);
#2431=VERTEX_POINT('',#9900);
#2432=VERTEX_POINT('',#9902);
#2433=VERTEX_POINT('',#9906);
#2434=VERTEX_POINT('',#9908);
#2435=VERTEX_POINT('',#9912);
#2436=VERTEX_POINT('',#9914);
#2437=VERTEX_POINT('',#9918);
#2438=VERTEX_POINT('',#9920);
#2964=EDGE_CURVE('',#2419,#2419,#2082,.T.);
#2965=EDGE_CURVE('',#2420,#2420,#2083,.T.);
#2966=EDGE_CURVE('',#2420,#2419,#1510,.T.);
#2967=EDGE_CURVE('',#2421,#2421,#2084,.T.);
#2968=EDGE_CURVE('',#2421,#2420,#1511,.T.);
#2969=EDGE_CURVE('',#2422,#2422,#2085,.T.);
#2970=EDGE_CURVE('',#2422,#2421,#1512,.T.);
#2971=EDGE_CURVE('',#2423,#2423,#2086,.T.);
#2972=EDGE_CURVE('',#2424,#2424,#2087,.F.);
#2973=EDGE_CURVE('',#2424,#2423,#1513,.T.);
#2974=EDGE_CURVE('',#2425,#2425,#2088,.F.);
#2975=EDGE_CURVE('',#2425,#2424,#1514,.T.);
#2976=EDGE_CURVE('',#2426,#2426,#2089,.T.);
#2977=EDGE_CURVE('',#2426,#2425,#1515,.T.);
#2978=EDGE_CURVE('',#2427,#2428,#1516,.T.);
#2979=EDGE_CURVE('',#2428,#2429,#1517,.T.);
#2980=EDGE_CURVE('',#2429,#2430,#1518,.T.);
#2981=EDGE_CURVE('',#2427,#2430,#1519,.T.);
#2982=EDGE_CURVE('',#2428,#2431,#1520,.T.);
#2983=EDGE_CURVE('',#2431,#2432,#1521,.T.);
#2984=EDGE_CURVE('',#2432,#2429,#1522,.T.);
#2985=EDGE_CURVE('',#2431,#2433,#1523,.T.);
#2986=EDGE_CURVE('',#2433,#2434,#1524,.T.);
#2987=EDGE_CURVE('',#2434,#2432,#1525,.T.);
#2988=EDGE_CURVE('',#2433,#2435,#1526,.T.);
#2989=EDGE_CURVE('',#2435,#2436,#1527,.T.);
#2990=EDGE_CURVE('',#2436,#2434,#1528,.T.);
#2991=EDGE_CURVE('',#2435,#2437,#1529,.T.);
#2992=EDGE_CURVE('',#2437,#2438,#1530,.T.);
#2993=EDGE_CURVE('',#2438,#2436,#1531,.T.);
#2994=EDGE_CURVE('',#2437,#2427,#1532,.T.);
#2995=EDGE_CURVE('',#2430,#2438,#1533,.T.);
#4017=ORIENTED_EDGE('',*,*,#2964,.F.);
#4018=ORIENTED_EDGE('',*,*,#2965,.F.);
#4019=ORIENTED_EDGE('',*,*,#2966,.T.);
#4020=ORIENTED_EDGE('',*,*,#2964,.T.);
#4021=ORIENTED_EDGE('',*,*,#2966,.F.);
#4022=ORIENTED_EDGE('',*,*,#2967,.F.);
#4023=ORIENTED_EDGE('',*,*,#2968,.T.);
#4024=ORIENTED_EDGE('',*,*,#2965,.T.);
#4025=ORIENTED_EDGE('',*,*,#2968,.F.);
#4026=ORIENTED_EDGE('',*,*,#2969,.F.);
#4027=ORIENTED_EDGE('',*,*,#2970,.T.);
#4028=ORIENTED_EDGE('',*,*,#2967,.T.);
#4029=ORIENTED_EDGE('',*,*,#2970,.F.);
#4030=ORIENTED_EDGE('',*,*,#2969,.T.);
#4031=ORIENTED_EDGE('',*,*,#2971,.F.);
#4032=ORIENTED_EDGE('',*,*,#2972,.F.);
#4033=ORIENTED_EDGE('',*,*,#2973,.T.);
#4034=ORIENTED_EDGE('',*,*,#2971,.T.);
#4035=ORIENTED_EDGE('',*,*,#2973,.F.);
#4036=ORIENTED_EDGE('',*,*,#2974,.F.);
#4037=ORIENTED_EDGE('',*,*,#2975,.T.);
#4038=ORIENTED_EDGE('',*,*,#2972,.T.);
#4039=ORIENTED_EDGE('',*,*,#2975,.F.);
#4040=ORIENTED_EDGE('',*,*,#2976,.F.);
#4041=ORIENTED_EDGE('',*,*,#2977,.T.);
#4042=ORIENTED_EDGE('',*,*,#2974,.T.);
#4043=ORIENTED_EDGE('',*,*,#2977,.F.);
#4044=ORIENTED_EDGE('',*,*,#2976,.T.);
#4045=ORIENTED_EDGE('',*,*,#2978,.T.);
#4046=ORIENTED_EDGE('',*,*,#2979,.T.);
#4047=ORIENTED_EDGE('',*,*,#2980,.T.);
#4048=ORIENTED_EDGE('',*,*,#2981,.F.);
#4049=ORIENTED_EDGE('',*,*,#2982,.T.);
#4050=ORIENTED_EDGE('',*,*,#2983,.T.);
#4051=ORIENTED_EDGE('',*,*,#2984,.T.);
#4052=ORIENTED_EDGE('',*,*,#2979,.F.);
#4053=ORIENTED_EDGE('',*,*,#2985,.T.);
#4054=ORIENTED_EDGE('',*,*,#2986,.T.);
#4055=ORIENTED_EDGE('',*,*,#2987,.T.);
#4056=ORIENTED_EDGE('',*,*,#2983,.F.);
#4057=ORIENTED_EDGE('',*,*,#2988,.T.);
#4058=ORIENTED_EDGE('',*,*,#2989,.T.);
#4059=ORIENTED_EDGE('',*,*,#2990,.T.);
#4060=ORIENTED_EDGE('',*,*,#2986,.F.);
#4061=ORIENTED_EDGE('',*,*,#2991,.T.);
#4062=ORIENTED_EDGE('',*,*,#2992,.T.);
#4063=ORIENTED_EDGE('',*,*,#2993,.T.);
#4064=ORIENTED_EDGE('',*,*,#2989,.F.);
#4065=ORIENTED_EDGE('',*,*,#2994,.T.);
#4066=ORIENTED_EDGE('',*,*,#2981,.T.);
#4067=ORIENTED_EDGE('',*,*,#2995,.T.);
#4068=ORIENTED_EDGE('',*,*,#2992,.F.);
#4069=ORIENTED_EDGE('',*,*,#2994,.F.);
#4070=ORIENTED_EDGE('',*,*,#2991,.F.);
#4071=ORIENTED_EDGE('',*,*,#2988,.F.);
#4072=ORIENTED_EDGE('',*,*,#2985,.F.);
#4073=ORIENTED_EDGE('',*,*,#2982,.F.);
#4074=ORIENTED_EDGE('',*,*,#2978,.F.);
#4075=ORIENTED_EDGE('',*,*,#2995,.F.);
#4076=ORIENTED_EDGE('',*,*,#2980,.F.);
#4077=ORIENTED_EDGE('',*,*,#2984,.F.);
#4078=ORIENTED_EDGE('',*,*,#2987,.F.);
#4079=ORIENTED_EDGE('',*,*,#2990,.F.);
#4080=ORIENTED_EDGE('',*,*,#2993,.F.);
#4397=CYLINDRICAL_SURFACE('',#5418,0.425);
#4398=CYLINDRICAL_SURFACE('',#5426,0.24505);
#4620=ADVANCED_FACE('',(#785),#524,.T.);
#4621=ADVANCED_FACE('',(#786),#170,.T.);
#4622=ADVANCED_FACE('',(#787),#4397,.T.);
#4623=ADVANCED_FACE('',(#788),#171,.T.);
#4624=ADVANCED_FACE('',(#789,#411),#525,.T.);
#4625=ADVANCED_FACE('',(#790),#172,.T.);
#4626=ADVANCED_FACE('',(#791),#4398,.T.);
#4627=ADVANCED_FACE('',(#792),#173,.T.);
#4628=ADVANCED_FACE('',(#793),#526,.T.);
#4629=ADVANCED_FACE('',(#794),#527,.F.);
#4630=ADVANCED_FACE('',(#795),#528,.F.);
#4631=ADVANCED_FACE('',(#796),#529,.F.);
#4632=ADVANCED_FACE('',(#797),#530,.F.);
#4633=ADVANCED_FACE('',(#798),#531,.F.);
#4634=ADVANCED_FACE('',(#799),#532,.F.);
#4635=ADVANCED_FACE('',(#800),#533,.F.);
#4636=ADVANCED_FACE('',(#801),#534,.F.);
#4707=CLOSED_SHELL('',(#4620,#4621,#4622,#4623,#4624,#4625,#4626,#4627,
#4628));
#4708=CLOSED_SHELL('',(#4629,#4630,#4631,#4632,#4633,#4634,#4635,#4636));
#5413=AXIS2_PLACEMENT_3D('',#9858,#6629,#6630);
#5414=AXIS2_PLACEMENT_3D('',#9859,#6631,#6632);
#5415=AXIS2_PLACEMENT_3D('',#9861,#6633,#6634);
#5416=AXIS2_PLACEMENT_3D('',#9862,#6635,#6636);
#5417=AXIS2_PLACEMENT_3D('',#9864,#6637,#6638);
#5418=AXIS2_PLACEMENT_3D('',#9866,#6640,#6641);
#5419=AXIS2_PLACEMENT_3D('',#9868,#6642,#6643);
#5420=AXIS2_PLACEMENT_3D('',#9870,#6645,#6646);
#5421=AXIS2_PLACEMENT_3D('',#9872,#6647,#6648);
#5422=AXIS2_PLACEMENT_3D('',#9874,#6650,#6651);
#5423=AXIS2_PLACEMENT_3D('',#9876,#6652,#6653);
#5424=AXIS2_PLACEMENT_3D('',#9877,#6654,#6655);
#5425=AXIS2_PLACEMENT_3D('',#9879,#6656,#6657);
#5426=AXIS2_PLACEMENT_3D('',#9881,#6659,#6660);
#5427=AXIS2_PLACEMENT_3D('',#9883,#6661,#6662);
#5428=AXIS2_PLACEMENT_3D('',#9885,#6664,#6665);
#5429=AXIS2_PLACEMENT_3D('',#9887,#6666,#6667);
#5430=AXIS2_PLACEMENT_3D('',#9889,#6669,#6670);
#5431=AXIS2_PLACEMENT_3D('',#9890,#6671,#6672);
#5432=AXIS2_PLACEMENT_3D('',#9899,#6677,#6678);
#5433=AXIS2_PLACEMENT_3D('',#9905,#6682,#6683);
#5434=AXIS2_PLACEMENT_3D('',#9911,#6687,#6688);
#5435=AXIS2_PLACEMENT_3D('',#9917,#6692,#6693);
#5436=AXIS2_PLACEMENT_3D('',#9923,#6697,#6698);
#5437=AXIS2_PLACEMENT_3D('',#9926,#6701,#6702);
#5438=AXIS2_PLACEMENT_3D('',#9927,#6703,#6704);
#6629=DIRECTION('axis',(0.,0.,1.));
#6630=DIRECTION('refdir',(1.,0.,0.));
#6631=DIRECTION('center_axis',(0.,1.,0.));
#6632=DIRECTION('ref_axis',(0.,0.,1.));
#6633=DIRECTION('center_axis',(0.,-1.,0.));
#6634=DIRECTION('ref_axis',(1.,0.,0.));
#6635=DIRECTION('center_axis',(0.,-1.,0.));
#6636=DIRECTION('ref_axis',(1.,0.,0.));
#6637=DIRECTION('center_axis',(0.,-1.,0.));
#6638=DIRECTION('ref_axis',(1.,0.,0.));
#6639=DIRECTION('',(0.707106781186548,0.707106781186547,8.65956056235493E-17));
#6640=DIRECTION('center_axis',(0.,-1.,0.));
#6641=DIRECTION('ref_axis',(1.,0.,0.));
#6642=DIRECTION('center_axis',(0.,-1.,0.));
#6643=DIRECTION('ref_axis',(1.,0.,0.));
#6644=DIRECTION('',(0.,1.,0.));
#6645=DIRECTION('center_axis',(0.,1.,0.));
#6646=DIRECTION('ref_axis',(1.,0.,0.));
#6647=DIRECTION('center_axis',(0.,-1.,0.));
#6648=DIRECTION('ref_axis',(1.,0.,0.));
#6649=DIRECTION('',(-0.707106781186547,0.707106781186548,-8.65956056235493E-17));
#6650=DIRECTION('center_axis',(0.,-1.,0.));
#6651=DIRECTION('ref_axis',(0.,0.,-1.));
#6652=DIRECTION('center_axis',(0.,-1.,0.));
#6653=DIRECTION('ref_axis',(1.,0.,0.));
#6654=DIRECTION('center_axis',(0.,1.,0.));
#6655=DIRECTION('ref_axis',(1.,0.,0.));
#6656=DIRECTION('center_axis',(0.,1.,0.));
#6657=DIRECTION('ref_axis',(1.,0.,0.));
#6658=DIRECTION('',(-0.447213595499958,0.894427190999916,-5.47678698264203E-17));
#6659=DIRECTION('center_axis',(0.,-1.,0.));
#6660=DIRECTION('ref_axis',(1.,0.,0.));
#6661=DIRECTION('center_axis',(0.,1.,0.));
#6662=DIRECTION('ref_axis',(1.,0.,0.));
#6663=DIRECTION('',(0.,1.,0.));
#6664=DIRECTION('center_axis',(0.,1.,0.));
#6665=DIRECTION('ref_axis',(1.,0.,0.));
#6666=DIRECTION('center_axis',(0.,-1.,0.));
#6667=DIRECTION('ref_axis',(1.,0.,0.));
#6668=DIRECTION('',(-0.707106781186547,0.707106781186548,-8.65956056235493E-17));
#6669=DIRECTION('center_axis',(0.,-1.,0.));
#6670=DIRECTION('ref_axis',(0.,0.,-1.));
#6671=DIRECTION('center_axis',(0.866025403784439,0.,-0.5));
#6672=DIRECTION('ref_axis',(0.5,0.,0.866025403784439));
#6673=DIRECTION('',(-0.5,0.,-0.866025403784439));
#6674=DIRECTION('',(0.,-1.,0.));
#6675=DIRECTION('',(0.5,0.,0.866025403784439));
#6676=DIRECTION('',(0.,-1.,0.));
#6677=DIRECTION('center_axis',(1.20185167898973E-16,0.,-1.));
#6678=DIRECTION('ref_axis',(1.,0.,1.20185167898973E-16));
#6679=DIRECTION('',(-1.,0.,-1.20185167898973E-16));
#6680=DIRECTION('',(0.,-1.,0.));
#6681=DIRECTION('',(1.,0.,1.20185167898973E-16));
#6682=DIRECTION('center_axis',(-0.866025403784439,0.,-0.5));
#6683=DIRECTION('ref_axis',(0.5,0.,-0.866025403784439));
#6684=DIRECTION('',(-0.5,0.,0.866025403784439));
#6685=DIRECTION('',(0.,-1.,0.));
#6686=DIRECTION('',(0.5,0.,-0.866025403784439));
#6687=DIRECTION('center_axis',(-0.866025403784439,0.,0.5));
#6688=DIRECTION('ref_axis',(-0.5,0.,-0.866025403784439));
#6689=DIRECTION('',(0.5,0.,0.866025403784439));
#6690=DIRECTION('',(0.,-1.,0.));
#6691=DIRECTION('',(-0.5,0.,-0.866025403784439));
#6692=DIRECTION('center_axis',(-2.40370335797945E-16,0.,1.));
#6693=DIRECTION('ref_axis',(-1.,0.,-2.40370335797945E-16));
#6694=DIRECTION('',(1.,0.,2.40370335797945E-16));
#6695=DIRECTION('',(0.,-1.,0.));
#6696=DIRECTION('',(-1.,0.,-2.40370335797945E-16));
#6697=DIRECTION('center_axis',(0.866025403784439,0.,0.5));
#6698=DIRECTION('ref_axis',(-0.5,0.,0.866025403784439));
#6699=DIRECTION('',(0.5,0.,-0.866025403784439));
#6700=DIRECTION('',(-0.5,0.,0.866025403784439));
#6701=DIRECTION('center_axis',(0.,1.,0.));
#6702=DIRECTION('ref_axis',(1.,0.,0.));
#6703=DIRECTION('center_axis',(0.,-1.,0.));
#6704=DIRECTION('ref_axis',(0.,0.,-1.));
#9858=CARTESIAN_POINT('',(0.,0.,0.));
#9859=CARTESIAN_POINT('Origin',(0.375,0.5,0.));
#9860=CARTESIAN_POINT('',(-0.375,0.5,-4.59242549680257E-17));
#9861=CARTESIAN_POINT('Origin',(0.,0.5,0.));
#9862=CARTESIAN_POINT('Origin',(0.,0.475,0.));
#9863=CARTESIAN_POINT('',(-0.425,0.45,-5.20474889637625E-17));
#9864=CARTESIAN_POINT('Origin',(0.,0.45,0.));
#9865=CARTESIAN_POINT('',(-0.4,0.475,-4.89858719658941E-17));
#9866=CARTESIAN_POINT('Origin',(0.,0.24,0.));
#9867=CARTESIAN_POINT('',(-0.425,0.0299999999999998,-5.20474889637625E-17));
#9868=CARTESIAN_POINT('Origin',(0.,0.0299999999999998,0.));
#9869=CARTESIAN_POINT('',(-0.425,0.24,-5.20474889637625E-17));
#9870=CARTESIAN_POINT('Origin',(0.,0.0150000000000001,0.));
#9871=CARTESIAN_POINT('',(-0.395,4.85722573273506E-17,-4.83735485663204E-17));
#9872=CARTESIAN_POINT('Origin',(0.,0.,0.));
#9873=CARTESIAN_POINT('',(-0.41,0.0150000000000001,-5.02105187650415E-17));
#9874=CARTESIAN_POINT('Origin',(0.27,0.,0.));
#9875=CARTESIAN_POINT('',(-0.27,0.,-3.30654635769785E-17));
#9876=CARTESIAN_POINT('Origin',(0.,0.,0.));
#9877=CARTESIAN_POINT('Origin',(0.,-0.02,0.));
#9878=CARTESIAN_POINT('',(-0.24505,-0.0498999999999999,3.00099698131059E-17));
#9879=CARTESIAN_POINT('Origin',(0.,-0.0498999999999999,0.));
#9880=CARTESIAN_POINT('',(-0.26,-0.02,-3.18408167778312E-17));
#9881=CARTESIAN_POINT('Origin',(0.,-0.995,0.));
#9882=CARTESIAN_POINT('',(-0.24505,-1.95495,3.00099698131059E-17));
#9883=CARTESIAN_POINT('Origin',(0.,-1.95495,0.));
#9884=CARTESIAN_POINT('',(-0.24505,-0.995,-3.00099698131059E-17));
#9885=CARTESIAN_POINT('Origin',(0.,-1.975,0.));
#9886=CARTESIAN_POINT('',(-0.2,-2.,-2.44929359829471E-17));
#9887=CARTESIAN_POINT('Origin',(0.,-2.,0.));
#9888=CARTESIAN_POINT('',(-0.225,-1.975,-2.75545529808154E-17));
#9889=CARTESIAN_POINT('Origin',(0.,-2.,0.));
#9890=CARTESIAN_POINT('Origin',(0.115470053837925,-0.5,-0.2));
#9891=CARTESIAN_POINT('',(0.23094010767585,-0.5,0.));
#9892=CARTESIAN_POINT('',(0.115470053837925,-0.5,-0.2));
#9893=CARTESIAN_POINT('',(0.23094010767585,-0.5,0.));
#9894=CARTESIAN_POINT('',(0.115470053837925,-0.8,-0.2));
#9895=CARTESIAN_POINT('',(0.115470053837925,-0.5,-0.2));
#9896=CARTESIAN_POINT('',(0.23094010767585,-0.8,0.));
#9897=CARTESIAN_POINT('',(0.23094010767585,-0.8,0.));
#9898=CARTESIAN_POINT('',(0.23094010767585,-0.5,0.));
#9899=CARTESIAN_POINT('Origin',(-0.115470053837925,-0.5,-0.2));
#9900=CARTESIAN_POINT('',(-0.115470053837925,-0.5,-0.2));
#9901=CARTESIAN_POINT('',(0.115470053837925,-0.5,-0.2));
#9902=CARTESIAN_POINT('',(-0.115470053837925,-0.8,-0.2));
#9903=CARTESIAN_POINT('',(-0.115470053837925,-0.5,-0.2));
#9904=CARTESIAN_POINT('',(0.115470053837925,-0.8,-0.2));
#9905=CARTESIAN_POINT('Origin',(-0.23094010767585,-0.5,-2.77555756156289E-17));
#9906=CARTESIAN_POINT('',(-0.23094010767585,-0.5,-2.82820063659975E-17));
#9907=CARTESIAN_POINT('',(-0.115470053837925,-0.5,-0.2));
#9908=CARTESIAN_POINT('',(-0.23094010767585,-0.8,-2.77555756156289E-17));
#9909=CARTESIAN_POINT('',(-0.23094010767585,-0.5,-2.82820063659975E-17));
#9910=CARTESIAN_POINT('',(-0.115470053837925,-0.8,-0.2));
#9911=CARTESIAN_POINT('Origin',(-0.115470053837925,-0.5,0.2));
#9912=CARTESIAN_POINT('',(-0.115470053837925,-0.5,0.2));
#9913=CARTESIAN_POINT('',(-0.23094010767585,-0.5,-2.82820063659975E-17));
#9914=CARTESIAN_POINT('',(-0.115470053837925,-0.8,0.2));
#9915=CARTESIAN_POINT('',(-0.115470053837925,-0.5,0.2));
#9916=CARTESIAN_POINT('',(-0.23094010767585,-0.8,-2.82820063659975E-17));
#9917=CARTESIAN_POINT('Origin',(0.115470053837925,-0.5,0.2));
#9918=CARTESIAN_POINT('',(0.115470053837925,-0.5,0.2));
#9919=CARTESIAN_POINT('',(-0.115470053837925,-0.5,0.2));
#9920=CARTESIAN_POINT('',(0.115470053837925,-0.8,0.2));
#9921=CARTESIAN_POINT('',(0.115470053837925,-0.5,0.2));
#9922=CARTESIAN_POINT('',(-0.115470053837925,-0.8,0.2));
#9923=CARTESIAN_POINT('Origin',(0.23094010767585,-0.5,0.));
#9924=CARTESIAN_POINT('',(0.115470053837925,-0.5,0.2));
#9925=CARTESIAN_POINT('',(0.115470053837925,-0.8,0.2));
#9926=CARTESIAN_POINT('Origin',(0.,-0.5,0.));
#9927=CARTESIAN_POINT('Origin',(0.,-0.8,0.));
#10234=UNCERTAINTY_MEASURE_WITH_UNIT(LENGTH_MEASURE(0.001),#10267,
'DISTANCE_ACCURACY_VALUE',
'Maximum model space distance between geometric entities at asserted c
onnectivities');
#10241=UNCERTAINTY_MEASURE_WITH_UNIT(LENGTH_MEASURE(0.001),#10267,
'DISTANCE_ACCURACY_VALUE',
'Maximum model space distance between geometric entities at asserted c
onnectivities');
#10259=(
GEOMETRIC_REPRESENTATION_CONTEXT(3)
GLOBAL_UNCERTAINTY_ASSIGNED_CONTEXT((#10234))
GLOBAL_UNIT_ASSIGNED_CONTEXT((#10267,#10269,#10270))
REPRESENTATION_CONTEXT('','3D')
);
#10266=(
GEOMETRIC_REPRESENTATION_CONTEXT(3)
GLOBAL_UNCERTAINTY_ASSIGNED_CONTEXT((#10241))
GLOBAL_UNIT_ASSIGNED_CONTEXT((#10267,#10269,#10270))
REPRESENTATION_CONTEXT('','3D')
);
#10267=(
LENGTH_UNIT()
NAMED_UNIT(*)
SI_UNIT(.CENTI.,.METRE.)
);
#10269=(
NAMED_UNIT(*)
PLANE_ANGLE_UNIT()
SI_UNIT($,.RADIAN.)
);
#10270=(
NAMED_UNIT(*)
SI_UNIT($,.STERADIAN.)
SOLID_ANGLE_UNIT()
);
#10288=SHAPE_DEFINITION_REPRESENTATION(#10312,#10371);
#10312=PRODUCT_DEFINITION_SHAPE('',$,#10396);
#10371=SHAPE_REPRESENTATION('',(#5413),#10259);
#10378=PRODUCT_DEFINITION_CONTEXT('part definition',#10452,'design');
#10396=PRODUCT_DEFINITION('Cap Screw - M5x20',
'Cap Screw - M5x20',#10420,#10378);
#10420=PRODUCT_DEFINITION_FORMATION('',$,#10471);
#10452=APPLICATION_CONTEXT(
'Core Data for Automotive Mechanical Design Process');
#10453=PRODUCT_CONTEXT('part definition',#10452,'mechanical');
#10471=PRODUCT('Cap Screw - M5x20','Cap Screw - M5x20',
'Cap Screw - M5x20',(#10453));
#10548=COLOUR_RGB('Black',0.12,0.14,0.17);
#10549=FILL_AREA_STYLE_COLOUR('',#10548);
#10550=FILL_AREA_STYLE('',(#10549));
#10551=SURFACE_STYLE_FILL_AREA(#10550);
#10552=SURFACE_SIDE_STYLE('',(#10551));
#10553=SURFACE_STYLE_USAGE(.BOTH.,#10552);
#10554=PRESENTATION_STYLE_ASSIGNMENT((#10553));
ENDSEC;
END-ISO-10303-21;
